ISO-10303-21;
HEADER;
/* Generated by software containing ST-Developer
 * from STEP Tools, Inc. (www.steptools.com) 
 */

FILE_DESCRIPTION(
/* description */ ('Dual-rail gantry carriage'),
/* implementation_level */ '2;1');

FILE_NAME(
/* name */ 'Cap Screw - M6x25.step',
/* time_stamp */ '2026-10-27T10:49:15-07:00',
/* author */ (''),
/* organization */ (''),
/* preprocessor_version */ 'ST-DEVELOPER v20.2',
/* originating_system */ 'Autodesk Translation Framework v15.17.0.0',
/* authorisation */ '');

FILE_SCHEMA (('AUTOMOTIVE_DESIGN { 1 0 10303 214 3 1 1 }'));
ENDSEC;

DATA;
#10=MECHANICAL_DESIGN_GEOMETRIC_PRESENTATION_REPRESENTATION('',(#613),#12804);
#496=ORIENTED_CLOSED_SHELL('',*,#7395,.F.);
#510=CONICAL_SURFACE('',#8382,0.475,0.785398163397449);
#511=CONICAL_SURFACE('',#8386,0.485,0.785398163397448);
#512=CONICAL_SURFACE('',#8390,0.31,0.463647609000806);
#513=CONICAL_SURFACE('',#8394,0.27,0.785398163397448);
#521=BREP_WITH_VOIDS('Body1',#7394,(#496));
#551=SHAPE_REPRESENTATION_RELATIONSHIP('SRR','None',#13031,#582);
#582=ADVANCED_BREP_SHAPE_REPRESENTATION('',(#521),#12801);
#613=STYLED_ITEM('',(#13254),#521);
#760=FACE_BOUND('',#1911,.T.);
#1024=PLANE('',#8380);
#1025=PLANE('',#8388);
#1026=PLANE('',#8396);
#1027=PLANE('',#8397);
#1028=PLANE('',#8398);
#1029=PLANE('',#8399);
#1030=PLANE('',#8400);
#1031=PLANE('',#8401);
#1032=PLANE('',#8402);
#1033=PLANE('',#8403);
#1034=PLANE('',#8404);
#1399=FACE_OUTER_BOUND('',#1906,.T.);
#1400=FACE_OUTER_BOUND('',#1907,.T.);
#1401=FACE_OUTER_BOUND('',#1908,.T.);
#1402=FACE_OUTER_BOUND('',#1909,.T.);
#1403=FACE_OUTER_BOUND('',#1910,.T.);
#1404=FACE_OUTER_BOUND('',#1912,.T.);
#1405=FACE_OUTER_BOUND('',#1913,.T.);
#1406=FACE_OUTER_BOUND('',#1914,.T.);
#1407=FACE_OUTER_BOUND('',#1915,.T.);
#1408=FACE_OUTER_BOUND('',#1916,.T.);
#1409=FACE_OUTER_BOUND('',#1917,.T.);
#1410=FACE_OUTER_BOUND('',#1918,.T.);
#1411=FACE_OUTER_BOUND('',#1919,.T.);
#1412=FACE_OUTER_BOUND('',#1920,.T.);
#1413=FACE_OUTER_BOUND('',#1921,.T.);
#1414=FACE_OUTER_BOUND('',#1922,.T.);
#1415=FACE_OUTER_BOUND('',#1923,.T.);
#1906=EDGE_LOOP('',(#6749));
#1907=EDGE_LOOP('',(#6750,#6751,#6752,#6753));
#1908=EDGE_LOOP('',(#6754,#6755,#6756,#6757));
#1909=EDGE_LOOP('',(#6758,#6759,#6760,#6761));
#1910=EDGE_LOOP('',(#6762));
#1911=EDGE_LOOP('',(#6763));
#1912=EDGE_LOOP('',(#6764,#6765,#6766,#6767));
#1913=EDGE_LOOP('',(#6768,#6769,#6770,#6771));
#1914=EDGE_LOOP('',(#6772,#6773,#6774,#6775));
#1915=EDGE_LOOP('',(#6776));
#1916=EDGE_LOOP('',(#6777,#6778,#6779,#6780));
#1917=EDGE_LOOP('',(#6781,#6782,#6783,#6784));
#1918=EDGE_LOOP('',(#6785,#6786,#6787,#6788));
#1919=EDGE_LOOP('',(#6789,#6790,#6791,#6792));
#1920=EDGE_LOOP('',(#6793,#6794,#6795,#6796));
#1921=EDGE_LOOP('',(#6797,#6798,#6799,#6800));
#1922=EDGE_LOOP('',(#6801,#6802,#6803,#6804,#6805,#6806));
#1923=EDGE_LOOP('',(#6807,#6808,#6809,#6810,#6811,#6812));
#2607=LINE('',#12538,#3316);
#2608=LINE('',#12542,#3317);
#2609=LINE('',#12546,#3318);
#2610=LINE('',#12553,#3319);
#2611=LINE('',#12557,#3320);
#2612=LINE('',#12561,#3321);
#2613=LINE('',#12566,#3322);
#2614=LINE('',#12568,#3323);
#2615=LINE('',#12570,#3324);
#2616=LINE('',#12571,#3325);
#2617=LINE('',#12574,#3326);
#2618=LINE('',#12576,#3327);
#2619=LINE('',#12577,#3328);
#2620=LINE('',#12580,#3329);
#2621=LINE('',#12582,#3330);
#2622=LINE('',#12583,#3331);
#2623=LINE('',#12586,#3332);
#2624=LINE('',#12588,#3333);
#2625=LINE('',#12589,#3334);
#2626=LINE('',#12592,#3335);
#2627=LINE('',#12594,#3336);
#2628=LINE('',#12595,#3337);
#2629=LINE('',#12597,#3338);
#2630=LINE('',#12598,#3339);
#3316=VECTOR('',#10432,0.475);
#3317=VECTOR('',#10437,0.5);
#3318=VECTOR('',#10442,0.485);
#3319=VECTOR('',#10451,0.31);
#3320=VECTOR('',#10456,0.3);
#3321=VECTOR('',#10461,0.27);
#3322=VECTOR('',#10466,1.);
#3323=VECTOR('',#10467,1.);
#3324=VECTOR('',#10468,1.);
#3325=VECTOR('',#10469,1.);
#3326=VECTOR('',#10472,1.);
#3327=VECTOR('',#10473,1.);
#3328=VECTOR('',#10474,1.);
#3329=VECTOR('',#10477,1.);
#3330=VECTOR('',#10478,1.);
#3331=VECTOR('',#10479,1.);
#3332=VECTOR('',#10482,1.);
#3333=VECTOR('',#10483,1.);
#3334=VECTOR('',#10484,1.);
#3335=VECTOR('',#10487,1.);
#3336=VECTOR('',#10488,1.);
#3337=VECTOR('',#10489,1.);
#3338=VECTOR('',#10492,1.);
#3339=VECTOR('',#10493,1.);
#3546=CIRCLE('',#8381,0.45);
#3547=CIRCLE('',#8383,0.5);
#3548=CIRCLE('',#8385,0.5);
#3549=CIRCLE('',#8387,0.47);
#3550=CIRCLE('',#8389,0.32);
#3551=CIRCLE('',#8391,0.2942);
#3552=CIRCLE('',#8393,0.2942);
#3553=CIRCLE('',#8395,0.24);
#4112=VERTEX_POINT('',#12533);
#4113=VERTEX_POINT('',#12536);
#4114=VERTEX_POINT('',#12540);
#4115=VERTEX_POINT('',#12544);
#4116=VERTEX_POINT('',#12548);
#4117=VERTEX_POINT('',#12551);
#4118=VERTEX_POINT('',#12555);
#4119=VERTEX_POINT('',#12559);
#4120=VERTEX_POINT('',#12564);
#4121=VERTEX_POINT('',#12565);
#4122=VERTEX_POINT('',#12567);
#4123=VERTEX_POINT('',#12569);
#4124=VERTEX_POINT('',#12573);
#4125=VERTEX_POINT('',#12575);
#4126=VERTEX_POINT('',#12579);
#4127=VERTEX_POINT('',#12581);
#4128=VERTEX_POINT('',#12585);
#4129=VERTEX_POINT('',#12587);
#4130=VERTEX_POINT('',#12591);
#4131=VERTEX_POINT('',#12593);
#4997=EDGE_CURVE('',#4112,#4112,#3546,.T.);
#4998=EDGE_CURVE('',#4113,#4113,#3547,.T.);
#4999=EDGE_CURVE('',#4113,#4112,#2607,.T.);
#5000=EDGE_CURVE('',#4114,#4114,#3548,.T.);
#5001=EDGE_CURVE('',#4114,#4113,#2608,.T.);
#5002=EDGE_CURVE('',#4115,#4115,#3549,.T.);
#5003=EDGE_CURVE('',#4115,#4114,#2609,.T.);
#5004=EDGE_CURVE('',#4116,#4116,#3550,.T.);
#5005=EDGE_CURVE('',#4117,#4117,#3551,.F.);
#5006=EDGE_CURVE('',#4117,#4116,#2610,.T.);
#5007=EDGE_CURVE('',#4118,#4118,#3552,.F.);
#5008=EDGE_CURVE('',#4118,#4117,#2611,.T.);
#5009=EDGE_CURVE('',#4119,#4119,#3553,.T.);
#5010=EDGE_CURVE('',#4119,#4118,#2612,.T.);
#5011=EDGE_CURVE('',#4120,#4121,#2613,.T.);
#5012=EDGE_CURVE('',#4121,#4122,#2614,.T.);
#5013=EDGE_CURVE('',#4122,#4123,#2615,.T.);
#5014=EDGE_CURVE('',#4120,#4123,#2616,.T.);
#5015=EDGE_CURVE('',#4121,#4124,#2617,.T.);
#5016=EDGE_CURVE('',#4124,#4125,#2618,.T.);
#5017=EDGE_CURVE('',#4125,#4122,#2619,.T.);
#5018=EDGE_CURVE('',#4124,#4126,#2620,.T.);
#5019=EDGE_CURVE('',#4126,#4127,#2621,.T.);
#5020=EDGE_CURVE('',#4127,#4125,#2622,.T.);
#5021=EDGE_CURVE('',#4126,#4128,#2623,.T.);
#5022=EDGE_CURVE('',#4128,#4129,#2624,.T.);
#5023=EDGE_CURVE('',#4129,#4127,#2625,.T.);
#5024=EDGE_CURVE('',#4128,#4130,#2626,.T.);
#5025=EDGE_CURVE('',#4130,#4131,#2627,.T.);
#5026=EDGE_CURVE('',#4131,#4129,#2628,.T.);
#5027=EDGE_CURVE('',#4130,#4120,#2629,.T.);
#5028=EDGE_CURVE('',#4123,#4131,#2630,.T.);
#6749=ORIENTED_EDGE('',*,*,#4997,.F.);
#6750=ORIENTED_EDGE('',*,*,#4998,.F.);
#6751=ORIENTED_EDGE('',*,*,#4999,.T.);
#6752=ORIENTED_EDGE('',*,*,#4997,.T.);
#6753=ORIENTED_EDGE('',*,*,#4999,.F.);
#6754=ORIENTED_EDGE('',*,*,#5000,.F.);
#6755=ORIENTED_EDGE('',*,*,#5001,.T.);
#6756=ORIENTED_EDGE('',*,*,#4998,.T.);
#6757=ORIENTED_EDGE('',*,*,#5001,.F.);
#6758=ORIENTED_EDGE('',*,*,#5002,.F.);
#6759=ORIENTED_EDGE('',*,*,#5003,.T.);
#6760=ORIENTED_EDGE('',*,*,#5000,.T.);
#6761=ORIENTED_EDGE('',*,*,#5003,.F.);
#6762=ORIENTED_EDGE('',*,*,#5002,.T.);
#6763=ORIENTED_EDGE('',*,*,#5004,.F.);
#6764=ORIENTED_EDGE('',*,*,#5005,.F.);
#6765=ORIENTED_EDGE('',*,*,#5006,.T.);
#6766=ORIENTED_EDGE('',*,*,#5004,.T.);
#6767=ORIENTED_EDGE('',*,*,#5006,.F.);
#6768=ORIENTED_EDGE('',*,*,#5007,.F.);
#6769=ORIENTED_EDGE('',*,*,#5008,.T.);
#6770=ORIENTED_EDGE('',*,*,#5005,.T.);
#6771=ORIENTED_EDGE('',*,*,#5008,.F.);
#6772=ORIENTED_EDGE('',*,*,#5009,.F.);
#6773=ORIENTED_EDGE('',*,*,#5010,.T.);
#6774=ORIENTED_EDGE('',*,*,#5007,.T.);
#6775=ORIENTED_EDGE('',*,*,#5010,.F.);
#6776=ORIENTED_EDGE('',*,*,#5009,.T.);
#6777=ORIENTED_EDGE('',*,*,#5011,.T.);
#6778=ORIENTED_EDGE('',*,*,#5012,.T.);
#6779=ORIENTED_EDGE('',*,*,#5013,.T.);
#6780=ORIENTED_EDGE('',*,*,#5014,.F.);
#6781=ORIENTED_EDGE('',*,*,#5015,.T.);
#6782=ORIENTED_EDGE('',*,*,#5016,.T.);
#6783=ORIENTED_EDGE('',*,*,#5017,.T.);
#6784=ORIENTED_EDGE('',*,*,#5012,.F.);
#6785=ORIENTED_EDGE('',*,*,#5018,.T.);
#6786=ORIENTED_EDGE('',*,*,#5019,.T.);
#6787=ORIENTED_EDGE('',*,*,#5020,.T.);
#6788=ORIENTED_EDGE('',*,*,#5016,.F.);
#6789=ORIENTED_EDGE('',*,*,#5021,.T.);
#6790=ORIENTED_EDGE('',*,*,#5022,.T.);
#6791=ORIENTED_EDGE('',*,*,#5023,.T.);
#6792=ORIENTED_EDGE('',*,*,#5019,.F.);
#6793=ORIENTED_EDGE('',*,*,#5024,.T.);
#6794=ORIENTED_EDGE('',*,*,#5025,.T.);
#6795=ORIENTED_EDGE('',*,*,#5026,.T.);
#6796=ORIENTED_EDGE('',*,*,#5022,.F.);
#6797=ORIENTED_EDGE('',*,*,#5027,.T.);
#6798=ORIENTED_EDGE('',*,*,#5014,.T.);
#6799=ORIENTED_EDGE('',*,*,#5028,.T.);
#6800=ORIENTED_EDGE('',*,*,#5025,.F.);
#6801=ORIENTED_EDGE('',*,*,#5027,.F.);
#6802=ORIENTED_EDGE('',*,*,#5024,.F.);
#6803=ORIENTED_EDGE('',*,*,#5021,.F.);
#6804=ORIENTED_EDGE('',*,*,#5018,.F.);
#6805=ORIENTED_EDGE('',*,*,#5015,.F.);
#6806=ORIENTED_EDGE('',*,*,#5011,.F.);
#6807=ORIENTED_EDGE('',*,*,#5028,.F.);
#6808=ORIENTED_EDGE('',*,*,#5013,.F.);
#6809=ORIENTED_EDGE('',*,*,#5017,.F.);
#6810=ORIENTED_EDGE('',*,*,#5020,.F.);
#6811=ORIENTED_EDGE('',*,*,#5023,.F.);
#6812=ORIENTED_EDGE('',*,*,#5026,.F.);
#6968=CYLINDRICAL_SURFACE('',#8384,0.5);
#6969=CYLINDRICAL_SURFACE('',#8392,0.2942);
#7325=ADVANCED_FACE('',(#1399),#1024,.T.);
#7326=ADVANCED_FACE('',(#1400),#510,.T.);
#7327=ADVANCED_FACE('',(#1401),#6968,.T.);
#7328=ADVANCED_FACE('',(#1402),#511,.T.);
#7329=ADVANCED_FACE('',(#1403,#760),#1025,.T.);
#7330=ADVANCED_FACE('',(#1404),#512,.T.);
#7331=ADVANCED_FACE('',(#1405),#6969,.T.);
#7332=ADVANCED_FACE('',(#1406),#513,.T.);
#7333=ADVANCED_FACE('',(#1407),#1026,.T.);
#7334=ADVANCED_FACE('',(#1408),#1027,.F.);
#7335=ADVANCED_FACE('',(#1409),#1028,.F.);
#7336=ADVANCED_FACE('',(#1410),#1029,.F.);
#7337=ADVANCED_FACE('',(#1411),#1030,.F.);
#7338=ADVANCED_FACE('',(#1412),#1031,.F.);
#7339=ADVANCED_FACE('',(#1413),#1032,.F.);
#7340=ADVANCED_FACE('',(#1414),#1033,.F.);
#7341=ADVANCED_FACE('',(#1415),#1034,.F.);
#7394=CLOSED_SHELL('',(#7325,#7326,#7327,#7328,#7329,#7330,#7331,#7332,
#7333));
#7395=CLOSED_SHELL('',(#7334,#7335,#7336,#7337,#7338,#7339,#7340,#7341));
#8379=AXIS2_PLACEMENT_3D('',#12531,#10422,#10423);
#8380=AXIS2_PLACEMENT_3D('',#12532,#10424,#10425);
#8381=AXIS2_PLACEMENT_3D('',#12534,#10426,#10427);
#8382=AXIS2_PLACEMENT_3D('',#12535,#10428,#10429);
#8383=AXIS2_PLACEMENT_3D('',#12537,#10430,#10431);
#8384=AXIS2_PLACEMENT_3D('',#12539,#10433,#10434);
#8385=AXIS2_PLACEMENT_3D('',#12541,#10435,#10436);
#8386=AXIS2_PLACEMENT_3D('',#12543,#10438,#10439);
#8387=AXIS2_PLACEMENT_3D('',#12545,#10440,#10441);
#8388=AXIS2_PLACEMENT_3D('',#12547,#10443,#10444);
#8389=AXIS2_PLACEMENT_3D('',#12549,#10445,#10446);
#8390=AXIS2_PLACEMENT_3D('',#12550,#10447,#10448);
#8391=AXIS2_PLACEMENT_3D('',#12552,#10449,#10450);
#8392=AXIS2_PLACEMENT_3D('',#12554,#10452,#10453);
#8393=AXIS2_PLACEMENT_3D('',#12556,#10454,#10455);
#8394=AXIS2_PLACEMENT_3D('',#12558,#10457,#10458);
#8395=AXIS2_PLACEMENT_3D('',#12560,#10459,#10460);
#8396=AXIS2_PLACEMENT_3D('',#12562,#10462,#10463);
#8397=AXIS2_PLACEMENT_3D('',#12563,#10464,#10465);
#8398=AXIS2_PLACEMENT_3D('',#12572,#10470,#10471);
#8399=AXIS2_PLACEMENT_3D('',#12578,#10475,#10476);
#8400=AXIS2_PLACEMENT_3D('',#12584,#10480,#10481);
#8401=AXIS2_PLACEMENT_3D('',#12590,#10485,#10486);
#8402=AXIS2_PLACEMENT_3D('',#12596,#10490,#10491);
#8403=AXIS2_PLACEMENT_3D('',#12599,#10494,#10495);
#8404=AXIS2_PLACEMENT_3D('',#12600,#10496,#10497);
#10422=DIRECTION('axis',(0.,0.,1.));
#10423=DIRECTION('refdir',(1.,0.,0.));
#10424=DIRECTION('center_axis',(0.,1.,0.));
#10425=DIRECTION('ref_axis',(0.,0.,1.));
#10426=DIRECTION('center_axis',(0.,-1.,0.));
#10427=DIRECTION('ref_axis',(1.,0.,0.));
#10428=DIRECTION('center_axis',(0.,-1.,0.));
#10429=DIRECTION('ref_axis',(1.,0.,0.));
#10430=DIRECTION('center_axis',(0.,-1.,0.));
#10431=DIRECTION('ref_axis',(1.,0.,0.));
#10432=DIRECTION('',(0.707106781186548,0.707106781186547,8.65956056235494E-17));
#10433=DIRECTION('center_axis',(0.,-1.,0.));
#10434=DIRECTION('ref_axis',(1.,0.,0.));
#10435=DIRECTION('center_axis',(0.,-1.,0.));
#10436=DIRECTION('ref_axis',(1.,0.,0.));
#10437=DIRECTION('',(0.,1.,0.));
#10438=DIRECTION('center_axis',(0.,1.,0.));
#10439=DIRECTION('ref_axis',(1.,0.,0.));
#10440=DIRECTION('center_axis',(0.,-1.,0.));
#10441=DIRECTION('ref_axis',(1.,0.,0.));
#10442=DIRECTION('',(-0.707106781186547,0.707106781186548,-8.65956056235493E-17));
#10443=DIRECTION('center_axis',(0.,-1.,0.));
#10444=DIRECTION('ref_axis',(0.,0.,-1.));
#10445=DIRECTION('center_axis',(0.,-1.,0.));
#10446=DIRECTION('ref_axis',(1.,0.,0.));
#10447=DIRECTION('center_axis',(0.,1.,0.));
#10448=DIRECTION('ref_axis',(1.,0.,0.));
#10449=DIRECTION('center_axis',(0.,1.,0.));
#10450=DIRECTION('ref_axis',(1.,0.,0.));
#10451=DIRECTION('',(-0.447213595499958,0.894427190999916,-5.47678698264203E-17));
#10452=DIRECTION('center_axis',(0.,-1.,0.));
#10453=DIRECTION('ref_axis',(1.,0.,0.));
#10454=DIRECTION('center_axis',(0.,1.,0.));
#10455=DIRECTION('ref_axis',(1.,0.,0.));
#10456=DIRECTION('',(0.,1.,0.));
#10457=DIRECTION('center_axis',(0.,1.,0.));
#10458=DIRECTION('ref_axis',(1.,0.,0.));
#10459=DIRECTION('center_axis',(0.,-1.,0.));
#10460=DIRECTION('ref_axis',(1.,0.,0.));
#10461=DIRECTION('',(-0.707106781186547,0.707106781186548,-8.65956056235493E-17));
#10462=DIRECTION('center_axis',(0.,-1.,0.));
#10463=DIRECTION('ref_axis',(0.,0.,-1.));
#10464=DIRECTION('center_axis',(0.866025403784439,0.,-0.5));
#10465=DIRECTION('ref_axis',(0.5,0.,0.866025403784439));
#10466=DIRECTION('',(-0.5,0.,-0.866025403784439));
#10467=DIRECTION('',(0.,-1.,0.));
#10468=DIRECTION('',(0.5,0.,0.866025403784439));
#10469=DIRECTION('',(0.,-1.,0.));
#10470=DIRECTION('center_axis',(1.92296268638356E-16,0.,-1.));
#10471=DIRECTION('ref_axis',(1.,0.,1.92296268638356E-16));
#10472=DIRECTION('',(-1.,0.,-1.92296268638356E-16));
#10473=DIRECTION('',(0.,-1.,0.));
#10474=DIRECTION('',(1.,0.,1.92296268638356E-16));
#10475=DIRECTION('center_axis',(-0.866025403784439,0.,-0.5));
#10476=DIRECTION('ref_axis',(0.5,0.,-0.866025403784439));
#10477=DIRECTION('',(-0.5,0.,0.866025403784438));
#10478=DIRECTION('',(0.,-1.,0.));
#10479=DIRECTION('',(0.5,0.,-0.866025403784438));
#10480=DIRECTION('center_axis',(-0.866025403784439,0.,0.5));
#10481=DIRECTION('ref_axis',(-0.5,0.,-0.866025403784439));
#10482=DIRECTION('',(0.5,0.,0.866025403784439));
#10483=DIRECTION('',(0.,-1.,0.));
#10484=DIRECTION('',(-0.5,0.,-0.866025403784439));
#10485=DIRECTION('center_axis',(-1.92296268638356E-16,0.,1.));
#10486=DIRECTION('ref_axis',(-1.,0.,-1.92296268638356E-16));
#10487=DIRECTION('',(1.,0.,1.92296268638356E-16));
#10488=DIRECTION('',(0.,-1.,0.));
#10489=DIRECTION('',(-1.,0.,-1.92296268638356E-16));
#10490=DIRECTION('center_axis',(0.866025403784439,0.,0.5));
#10491=DIRECTION('ref_axis',(-0.5,0.,0.866025403784439));
#10492=DIRECTION('',(0.5,0.,-0.866025403784439));
#10493=DIRECTION('',(-0.5,0.,0.866025403784439));
#10494=DIRECTION('center_axis',(0.,1.,0.));
#10495=DIRECTION('ref_axis',(1.,0.,0.));
#10496=DIRECTION('center_axis',(0.,-1.,0.));
#10497=DIRECTION('ref_axis',(0.,0.,-1.));
#12531=CARTESIAN_POINT('',(0.,0.,0.));
#12532=CARTESIAN_POINT('Origin',(0.45,0.6,0.));
#12533=CARTESIAN_POINT('',(-0.45,0.6,-5.51091059616309E-17));
#12534=CARTESIAN_POINT('Origin',(0.,0.6,0.));
#12535=CARTESIAN_POINT('Origin',(0.,0.575,0.));
#12536=CARTESIAN_POINT('',(-0.5,0.55,-6.12323399573677E-17));
#12537=CARTESIAN_POINT('Origin',(0.,0.55,0.));
#12538=CARTESIAN_POINT('',(-0.475,0.575,-5.81707229594993E-17));
#12539=CARTESIAN_POINT('Origin',(0.,0.29,0.));
#12540=CARTESIAN_POINT('',(-0.5,0.0299999999999998,-6.12323399573677E-17));
#12541=CARTESIAN_POINT('Origin',(0.,0.0299999999999998,0.));
#12542=CARTESIAN_POINT('',(-0.5,0.29,-6.12323399573677E-17));
#12543=CARTESIAN_POINT('Origin',(0.,0.0150000000000001,0.));
#12544=CARTESIAN_POINT('',(-0.47,7.11236625150491E-17,-5.75583995599256E-17));
#12545=CARTESIAN_POINT('Origin',(0.,0.,0.));
#12546=CARTESIAN_POINT('',(-0.485,0.0150000000000001,-5.93953697586466E-17));
#12547=CARTESIAN_POINT('Origin',(0.32,0.,0.));
#12548=CARTESIAN_POINT('',(-0.32,-6.93889390390723E-18,-3.91886975727153E-17));
#12549=CARTESIAN_POINT('Origin',(0.,0.,0.));
#12550=CARTESIAN_POINT('Origin',(0.,-0.02,0.));
#12551=CARTESIAN_POINT('',(-0.2942,-0.0515999999999999,3.60291088309151E-17));
#12552=CARTESIAN_POINT('Origin',(0.,-0.0515999999999999,0.));
#12553=CARTESIAN_POINT('',(-0.31,-0.02,-3.7964050773568E-17));
#12554=CARTESIAN_POINT('Origin',(0.,-1.24,0.));
#12555=CARTESIAN_POINT('',(-0.2942,-2.4458,3.60291088309151E-17));
#12556=CARTESIAN_POINT('Origin',(0.,-2.4458,0.));
#12557=CARTESIAN_POINT('',(-0.2942,-1.24,-3.60291088309151E-17));
#12558=CARTESIAN_POINT('Origin',(0.,-2.47,0.));
#12559=CARTESIAN_POINT('',(-0.24,-2.5,-2.93915231795365E-17));
#12560=CARTESIAN_POINT('Origin',(0.,-2.5,0.));
#12561=CARTESIAN_POINT('',(-0.27,-2.47,-3.30654635769785E-17));
#12562=CARTESIAN_POINT('Origin',(0.,-2.5,0.));
#12563=CARTESIAN_POINT('Origin',(0.144337567297406,-0.6,-0.25));
#12564=CARTESIAN_POINT('',(0.288675134594813,-0.6,0.));
#12565=CARTESIAN_POINT('',(0.144337567297406,-0.6,-0.25));
#12566=CARTESIAN_POINT('',(0.288675134594813,-0.6,0.));
#12567=CARTESIAN_POINT('',(0.144337567297406,-0.96,-0.25));
#12568=CARTESIAN_POINT('',(0.144337567297406,-0.6,-0.25));
#12569=CARTESIAN_POINT('',(0.288675134594813,-0.96,0.));
#12570=CARTESIAN_POINT('',(0.288675134594813,-0.96,0.));
#12571=CARTESIAN_POINT('',(0.288675134594813,-0.6,0.));
#12572=CARTESIAN_POINT('Origin',(-0.144337567297406,-0.6,-0.25));
#12573=CARTESIAN_POINT('',(-0.144337567297406,-0.6,-0.25));
#12574=CARTESIAN_POINT('',(0.144337567297406,-0.6,-0.25));
#12575=CARTESIAN_POINT('',(-0.144337567297406,-0.96,-0.25));
#12576=CARTESIAN_POINT('',(-0.144337567297406,-0.6,-0.25));
#12577=CARTESIAN_POINT('',(0.144337567297406,-0.96,-0.25));
#12578=CARTESIAN_POINT('Origin',(-0.288675134594813,-0.6,-8.32667268468867E-17));
#12579=CARTESIAN_POINT('',(-0.288675134594813,-0.6,-3.53525079574969E-17));
#12580=CARTESIAN_POINT('',(-0.144337567297406,-0.6,-0.25));
#12581=CARTESIAN_POINT('',(-0.288675134594813,-0.96,-5.55111512312578E-17));
#12582=CARTESIAN_POINT('',(-0.288675134594813,-0.6,-3.53525079574969E-17));
#12583=CARTESIAN_POINT('',(-0.144337567297406,-0.96,-0.25));
#12584=CARTESIAN_POINT('Origin',(-0.144337567297407,-0.6,0.25));
#12585=CARTESIAN_POINT('',(-0.144337567297407,-0.6,0.25));
#12586=CARTESIAN_POINT('',(-0.288675134594813,-0.6,-3.53525079574969E-17));
#12587=CARTESIAN_POINT('',(-0.144337567297407,-0.96,0.25));
#12588=CARTESIAN_POINT('',(-0.144337567297407,-0.6,0.25));
#12589=CARTESIAN_POINT('',(-0.288675134594813,-0.96,-3.53525079574969E-17));
#12590=CARTESIAN_POINT('Origin',(0.144337567297406,-0.6,0.25));
#12591=CARTESIAN_POINT('',(0.144337567297406,-0.6,0.25));
#12592=CARTESIAN_POINT('',(-0.144337567297407,-0.6,0.25));
#12593=CARTESIAN_POINT('',(0.144337567297406,-0.96,0.25));
#12594=CARTESIAN_POINT('',(0.144337567297406,-0.6,0.25));
#12595=CARTESIAN_POINT('',(-0.144337567297407,-0.96,0.25));
#12596=CARTESIAN_POINT('Origin',(0.288675134594813,-0.6,0.));
#12597=CARTESIAN_POINT('',(0.144337567297406,-0.6,0.25));
#12598=CARTESIAN_POINT('',(0.144337567297406,-0.96,0.25));
#12599=CARTESIAN_POINT('Origin',(0.,-0.6,0.));
#12600=CARTESIAN_POINT('Origin',(0.,-0.96,0.));
#12765=UNCERTAINTY_MEASURE_WITH_UNIT(LENGTH_MEASURE(0.001),#12805,
'DISTANCE_ACCURACY_VALUE',
'Maximum model space distance between geometric entities at asserted c
onnectivities');
#12768=UNCERTAINTY_MEASURE_WITH_UNIT(LENGTH_MEASURE(0.001),#12805,
'DISTANCE_ACCURACY_VALUE',
'Maximum model space distance between geometric entities at asserted c
onnectivities');
#12801=(
GEOMETRIC_REPRESENTATION_CONTEXT(3)
GLOBAL_UNCERTAINTY_ASSIGNED_CONTEXT((#12765))
GLOBAL_UNIT_ASSIGNED_CONTEXT((#12805,#12807,#12808))
REPRESENTATION_CONTEXT('','3D')
);
#12804=(
GEOMETRIC_REPRESENTATION_CONTEXT(3)
GLOBAL_UNCERTAINTY_ASSIGNED_CONTEXT((#12768))
GLOBAL_UNIT_ASSIGNED_CONTEXT((#12805,#12807,#12808))
REPRESENTATION_CONTEXT('','3D')
);
#12805=(
LENGTH_UNIT()
NAMED_UNIT(*)
SI_UNIT(.CENTI.,.METRE.)
);
#12807=(
NAMED_UNIT(*)
PLANE_ANGLE_UNIT()
SI_UNIT($,.RADIAN.)
);
#12808=(
NAMED_UNIT(*)
SI_UNIT($,.STERADIAN.)
SOLID_ANGLE_UNIT()
);
#12841=SHAPE_DEFINITION_REPRESENTATION(#12949,#13031);
#12949=PRODUCT_DEFINITION_SHAPE('',$,#13067);
#13031=SHAPE_REPRESENTATION('',(#8379),#12801);
#13034=PRODUCT_DEFINITION_CONTEXT('part definition',#13141,'design');
#13067=PRODUCT_DEFINITION('Cap Screw - M6x25','Cap Screw - M6x25',#13102,
#13034);
#13102=PRODUCT_DEFINITION_FORMATION('',$,#13175);
#13141=APPLICATION_CONTEXT(
'Core Data for Automotive Mechanical Design Process');
#13142=PRODUCT_CONTEXT('part definition',#13141,'mechanical');
#13175=PRODUCT('Cap Screw - M6x25','Cap Screw - M6x25',
'Cap Screw - M6x25',(#13142));
#13248=COLOUR_RGB('Black',0.12,0.14,0.17);
#13249=FILL_AREA_STYLE_COLOUR('',#13248);
#13250=FILL_AREA_STYLE('',(#13249));
#13251=SURFACE_STYLE_FILL_AREA(#13250);
#13252=SURFACE_SIDE_STYLE('',(#13251));
#13253=SURFACE_STYLE_USAGE(.BOTH.,#13252);
#13254=PRESENTATION_STYLE_ASSIGNMENT((#13253));
ENDSEC;
END-ISO-10303-21;
